ISO-10303-21;
HEADER;
/* Generated by software containing ST-Developer
 * from STEP Tools, Inc. (www.steptools.com) 
 */

FILE_DESCRIPTION(
/* description */ ('Torque wrench calibration arm'),
/* implementation_level */ '2;1');

FILE_NAME(
/* name */ 'Hanger inner spacer (1).step',
/* time_stamp */ '2026-10-28T03:24:52-07:00',
/* author */ (''),
/* organization */ (''),
/* preprocessor_version */ 'ST-DEVELOPER v20.2',
/* originating_system */ 'Autodesk Translation Framework v15.17.0.0',
/* authorisation */ '');

FILE_SCHEMA (('AUTOMOTIVE_DESIGN { 1 0 10303 214 3 1 1 }'));
ENDSEC;

DATA;
#10=MECHANICAL_DESIGN_GEOMETRIC_PRESENTATION_REPRESENTATION('',(#474),#12783);
#383=SHAPE_REPRESENTATION_RELATIONSHIP('SRR','None',#12968,#420);
#420=ADVANCED_BREP_SHAPE_REPRESENTATION('',(#526),#12777);
#474=STYLED_ITEM('',(#13205),#526);
#526=MANIFOLD_SOLID_BREP('Body1',#6545);
#641=FACE_BOUND('',#1742,.T.);
#642=FACE_BOUND('',#1744,.T.);
#854=PLANE('',#7735);
#855=PLANE('',#7736);
#1234=FACE_OUTER_BOUND('',#1739,.T.);
#1235=FACE_OUTER_BOUND('',#1740,.T.);
#1236=FACE_OUTER_BOUND('',#1741,.T.);
#1237=FACE_OUTER_BOUND('',#1743,.T.);
#1739=EDGE_LOOP('',(#5867,#5868,#5869,#5870));
#1740=EDGE_LOOP('',(#5871,#5872,#5873,#5874));
#1741=EDGE_LOOP('',(#5875));
#1742=EDGE_LOOP('',(#5876));
#1743=EDGE_LOOP('',(#5877));
#1744=EDGE_LOOP('',(#5878));
#2168=LINE('',#12547,#2583);
#2169=LINE('',#12553,#2584);
#2583=VECTOR('',#9734,0.505000000000003);
#2584=VECTOR('',#9741,0.700000000000003);
#2944=CIRCLE('',#7730,0.505000000000003);
#2945=CIRCLE('',#7731,0.505000000000003);
#2946=CIRCLE('',#7733,0.700000000000003);
#2947=CIRCLE('',#7734,0.700000000000003);
#3494=VERTEX_POINT('',#12544);
#3495=VERTEX_POINT('',#12546);
#3496=VERTEX_POINT('',#12550);
#3497=VERTEX_POINT('',#12552);
#4291=EDGE_CURVE('',#3494,#3494,#2944,.T.);
#4292=EDGE_CURVE('',#3494,#3495,#2168,.T.);
#4293=EDGE_CURVE('',#3495,#3495,#2945,.T.);
#4294=EDGE_CURVE('',#3496,#3496,#2946,.T.);
#4295=EDGE_CURVE('',#3496,#3497,#2169,.T.);
#4296=EDGE_CURVE('',#3497,#3497,#2947,.T.);
#5867=ORIENTED_EDGE('',*,*,#4291,.F.);
#5868=ORIENTED_EDGE('',*,*,#4292,.T.);
#5869=ORIENTED_EDGE('',*,*,#4293,.T.);
#5870=ORIENTED_EDGE('',*,*,#4292,.F.);
#5871=ORIENTED_EDGE('',*,*,#4294,.F.);
#5872=ORIENTED_EDGE('',*,*,#4295,.T.);
#5873=ORIENTED_EDGE('',*,*,#4296,.T.);
#5874=ORIENTED_EDGE('',*,*,#4295,.F.);
#5875=ORIENTED_EDGE('',*,*,#4294,.T.);
#5876=ORIENTED_EDGE('',*,*,#4291,.T.);
#5877=ORIENTED_EDGE('',*,*,#4296,.F.);
#5878=ORIENTED_EDGE('',*,*,#4293,.F.);
#6088=CYLINDRICAL_SURFACE('',#7729,0.505000000000003);
#6089=CYLINDRICAL_SURFACE('',#7732,0.700000000000003);
#6459=ADVANCED_FACE('',(#1234),#6088,.F.);
#6460=ADVANCED_FACE('',(#1235),#6089,.T.);
#6461=ADVANCED_FACE('',(#1236,#641),#854,.T.);
#6462=ADVANCED_FACE('',(#1237,#642),#855,.F.);
#6545=CLOSED_SHELL('',(#6459,#6460,#6461,#6462));
#7728=AXIS2_PLACEMENT_3D('',#12542,#9728,#9729);
#7729=AXIS2_PLACEMENT_3D('',#12543,#9730,#9731);
#7730=AXIS2_PLACEMENT_3D('',#12545,#9732,#9733);
#7731=AXIS2_PLACEMENT_3D('',#12548,#9735,#9736);
#7732=AXIS2_PLACEMENT_3D('',#12549,#9737,#9738);
#7733=AXIS2_PLACEMENT_3D('',#12551,#9739,#9740);
#7734=AXIS2_PLACEMENT_3D('',#12554,#9742,#9743);
#7735=AXIS2_PLACEMENT_3D('',#12555,#9744,#9745);
#7736=AXIS2_PLACEMENT_3D('',#12556,#9746,#9747);
#9728=DIRECTION('axis',(0.,0.,1.));
#9729=DIRECTION('refdir',(1.,0.,0.));
#9730=DIRECTION('center_axis',(0.,1.,0.));
#9731=DIRECTION('ref_axis',(1.,0.,0.));
#9732=DIRECTION('center_axis',(0.,-1.,0.));
#9733=DIRECTION('ref_axis',(1.,0.,0.));
#9734=DIRECTION('',(0.,-1.,0.));
#9735=DIRECTION('center_axis',(0.,-1.,0.));
#9736=DIRECTION('ref_axis',(1.,0.,0.));
#9737=DIRECTION('center_axis',(0.,1.,0.));
#9738=DIRECTION('ref_axis',(1.,0.,0.));
#9739=DIRECTION('center_axis',(0.,1.,0.));
#9740=DIRECTION('ref_axis',(1.,0.,0.));
#9741=DIRECTION('',(0.,-1.,0.));
#9742=DIRECTION('center_axis',(0.,1.,0.));
#9743=DIRECTION('ref_axis',(1.,0.,0.));
#9744=DIRECTION('center_axis',(0.,1.,0.));
#9745=DIRECTION('ref_axis',(1.,0.,0.));
#9746=DIRECTION('center_axis',(0.,1.,0.));
#9747=DIRECTION('ref_axis',(1.,0.,0.));
#12542=CARTESIAN_POINT('',(0.,0.,0.));
#12543=CARTESIAN_POINT('Origin',(50.,8.95,8.));
#12544=CARTESIAN_POINT('',(49.495,9.7,8.));
#12545=CARTESIAN_POINT('Origin',(50.,9.7,8.));
#12546=CARTESIAN_POINT('',(49.495,8.95,8.));
#12547=CARTESIAN_POINT('',(49.495,8.95,8.));
#12548=CARTESIAN_POINT('Origin',(50.,8.95,8.));
#12549=CARTESIAN_POINT('Origin',(50.,8.95,8.));
#12550=CARTESIAN_POINT('',(49.3,9.7,8.));
#12551=CARTESIAN_POINT('Origin',(50.,9.7,8.));
#12552=CARTESIAN_POINT('',(49.3,8.95,8.));
#12553=CARTESIAN_POINT('',(49.3,8.95,8.));
#12554=CARTESIAN_POINT('Origin',(50.,8.95,8.));
#12555=CARTESIAN_POINT('Origin',(50.,9.7,8.));
#12556=CARTESIAN_POINT('Origin',(50.,8.95,8.));
#12733=UNCERTAINTY_MEASURE_WITH_UNIT(LENGTH_MEASURE(0.001),#12784,
'DISTANCE_ACCURACY_VALUE',
'Maximum model space distance between geometric entities at asserted c
onnectivities');
#12739=UNCERTAINTY_MEASURE_WITH_UNIT(LENGTH_MEASURE(0.001),#12784,
'DISTANCE_ACCURACY_VALUE',
'Maximum model space distance between geometric entities at asserted c
onnectivities');
#12777=(
GEOMETRIC_REPRESENTATION_CONTEXT(3)
GLOBAL_UNCERTAINTY_ASSIGNED_CONTEXT((#12733))
GLOBAL_UNIT_ASSIGNED_CONTEXT((#12784,#12786,#12787))
REPRESENTATION_CONTEXT('','3D')
);
#12783=(
GEOMETRIC_REPRESENTATION_CONTEXT(3)
GLOBAL_UNCERTAINTY_ASSIGNED_CONTEXT((#12739))
GLOBAL_UNIT_ASSIGNED_CONTEXT((#12784,#12786,#12787))
REPRESENTATION_CONTEXT('','3D')
);
#12784=(
LENGTH_UNIT()
NAMED_UNIT(*)
SI_UNIT(.CENTI.,.METRE.)
);
#12786=(
NAMED_UNIT(*)
PLANE_ANGLE_UNIT()
SI_UNIT($,.RADIAN.)
);
#12787=(
NAMED_UNIT(*)
SI_UNIT($,.STERADIAN.)
SOLID_ANGLE_UNIT()
);
#12825=SHAPE_DEFINITION_REPRESENTATION(#12912,#12968);
#12912=PRODUCT_DEFINITION_SHAPE('',$,#13012);
#12968=SHAPE_REPRESENTATION('',(#7728),#12777);
#12974=PRODUCT_DEFINITION_CONTEXT('part definition',#13105,'design');
#13012=PRODUCT_DEFINITION('Hanger inner spacer (1)',
'Hanger inner spacer (1)',#13055,#12974);
#13055=PRODUCT_DEFINITION_FORMATION('',$,#13144);
#13105=APPLICATION_CONTEXT(
'Core Data for Automotive Mechanical Design Process');
#13106=PRODUCT_CONTEXT('part definition',#13105,'mechanical');
#13144=PRODUCT('Hanger inner spacer (1)','Hanger inner spacer (1)',
'Hanger inner spacer (1)',(#13106));
#13199=COLOUR_RGB('Sky Blue',0.24,0.69,0.87);
#13200=FILL_AREA_STYLE_COLOUR('',#13199);
#13201=FILL_AREA_STYLE('',(#13200));
#13202=SURFACE_STYLE_FILL_AREA(#13201);
#13203=SURFACE_SIDE_STYLE('',(#13202));
#13204=SURFACE_STYLE_USAGE(.BOTH.,#13203);
#13205=PRESENTATION_STYLE_ASSIGNMENT((#13204));
ENDSEC;
END-ISO-10303-21;
